ISO-10303-21;
HEADER;
FILE_DESCRIPTION (('STEP AP214'),
    '1' );
FILE_NAME ('plain washer (type a)_is_IS 2016 A- 22.step',
    '2026-10-26T19:46:16',
    ( '' ),
    ( '' ),
    'SwSTEP 2.0',
    'SolidWorks 2025',
    '' );
FILE_SCHEMA (( 'AUTOMOTIVE_DESIGN' ));
ENDSEC;

DATA;
#36=EDGE_CURVE ( 'NONE', #35937, #61038, #73180, .T. ) ;
#1071=PLANE ( 'NONE',  #13150 ) ;
#1746=CYLINDRICAL_SURFACE ( 'NONE', #73756, 11.00000000000000000 ) ;
#1968=( GEOMETRIC_REPRESENTATION_CONTEXT ( 3 ) GLOBAL_UNCERTAINTY_ASSIGNED_CONTEXT ( ( #64509 ) ) GLOBAL_UNIT_ASSIGNED_CONTEXT ( ( #4941, #10591, #68299 ) ) REPRESENTATION_CONTEXT ( 'NONE', 'WORKASPACE' ) );
#2536=ORIENTED_EDGE ( 'NONE', *, *, #58834, .T. ) ;
#2710=AXIS2_PLACEMENT_3D ( 'NONE', #8838, #54872, #72586 ) ;
#2815=CARTESIAN_POINT ( 'NONE',  ( 0.000000000000000000, 0.000000000000000000, 0.000000000000000000 ) ) ;
#4264=EDGE_LOOP ( 'NONE', ( #42185, #33044 ) ) ;
#4362=EDGE_LOOP ( 'NONE', ( #48334, #61367 ) ) ;
#4696=VECTOR ( 'NONE', #32247, 1000.000000000000000 ) ;
#4941=( LENGTH_UNIT ( ) NAMED_UNIT ( * ) SI_UNIT ( .MILLI., .METRE. ) );
#5423=( LENGTH_UNIT ( ) NAMED_UNIT ( * ) SI_UNIT ( .MILLI., .METRE. ) );
#5748=EDGE_LOOP ( 'NONE', ( #17016, #60402, #16082, #67832 ) ) ;
#5893=DIRECTION ( 'NONE',  ( 0.000000000000000000, 0.000000000000000000, 1.000000000000000000 ) ) ;
#6220=EDGE_CURVE ( 'NONE', #25826, #26283, #73624, .T. ) ;
#7401=FACE_OUTER_BOUND ( 'NONE', #60574, .T. ) ;
#7933=CARTESIAN_POINT ( 'NONE',  ( 0.000000000000000000, 0.000000000000000000, 18.50000000000000000 ) ) ;
#8379=AXIS2_PLACEMENT_3D ( 'NONE', #8501, #36442, #36809 ) ;
#8501=CARTESIAN_POINT ( 'NONE',  ( 0.000000000000000000, 0.000000000000000000, 0.000000000000000000 ) ) ;
#8838=CARTESIAN_POINT ( 'NONE',  ( 0.000000000000000000, -3.149999999999999911, 0.000000000000000000 ) ) ;
#9398=CARTESIAN_POINT ( 'NONE',  ( 0.000000000000000000, -3.149999999999999911, 18.50000000000000000 ) ) ;
#9796=ORIENTED_EDGE ( 'NONE', *, *, #6220, .F. ) ;
#10471=CARTESIAN_POINT ( 'NONE',  ( 0.000000000000000000, -3.149999999999999911, 0.000000000000000000 ) ) ;
#10591=( NAMED_UNIT ( * ) PLANE_ANGLE_UNIT ( ) SI_UNIT ( $, .RADIAN. ) );
#10937=AXIS2_PLACEMENT_3D ( 'NONE', #14161, #42471, #54185 ) ;
#11422=DIRECTION ( 'NONE',  ( 0.000000000000000000, 0.000000000000000000, 1.000000000000000000 ) ) ;
#11625=DIRECTION ( 'NONE',  ( -0.000000000000000000, 1.000000000000000000, 0.000000000000000000 ) ) ;
#12100=DIRECTION ( 'NONE',  ( -0.000000000000000000, 1.000000000000000000, -0.000000000000000000 ) ) ;
#12135=UNCERTAINTY_MEASURE_WITH_UNIT (LENGTH_MEASURE( 1.000000000000000082E-05 ), #5423, 'distance_accuracy_value', 'NONE');
#12365=CARTESIAN_POINT ( 'NONE',  ( 11.00000000000000000, 0.000000000000000000, 0.000000000000000000 ) ) ;
#13150=AXIS2_PLACEMENT_3D ( 'NONE', #12365, #11625, #56918 ) ;
#13759=CARTESIAN_POINT ( 'NONE',  ( 2.265596578422603396E-15, 0.000000000000000000, -18.50000000000000000 ) ) ;
#14161=CARTESIAN_POINT ( 'NONE',  ( 0.000000000000000000, 0.000000000000000000, 0.000000000000000000 ) ) ;
#14572=DIRECTION ( 'NONE',  ( 0.000000000000000000, 0.000000000000000000, 1.000000000000000000 ) ) ;
#14600=CIRCLE ( 'NONE', #2710, 18.50000000000000000 ) ;
#15017=PRODUCT_DEFINITION ( 'UNKNOWN', '', #61044, #68940 ) ;
#16082=ORIENTED_EDGE ( 'NONE', *, *, #6220, .T. ) ;
#16956=CIRCLE ( 'NONE', #10937, 11.00000000000000000 ) ;
#17016=ORIENTED_EDGE ( 'NONE', *, *, #53272, .F. ) ;
#18030=FACE_OUTER_BOUND ( 'NONE', #4362, .T. ) ;
#18099=ORIENTED_EDGE ( 'NONE', *, *, #71135, .F. ) ;
#18155=FACE_OUTER_BOUND ( 'NONE', #5748, .T. ) ;
#19076=DIRECTION ( 'NONE',  ( 0.000000000000000000, 0.000000000000000000, 1.000000000000000000 ) ) ;
#20010=VERTEX_POINT ( 'NONE', #47453 ) ;
#21124=DIRECTION ( 'NONE',  ( 0.000000000000000000, -1.000000000000000000, 0.000000000000000000 ) ) ;
#21274=DIRECTION ( 'NONE',  ( 0.000000000000000000, 0.000000000000000000, 1.000000000000000000 ) ) ;
#21905=LINE ( 'NONE', #39273, #48221 ) ;
#22145=DIRECTION ( 'NONE',  ( 0.000000000000000000, 0.000000000000000000, 1.000000000000000000 ) ) ;
#23815=CYLINDRICAL_SURFACE ( 'NONE', #33711, 11.00000000000000000 ) ;
#24098=CARTESIAN_POINT ( 'NONE',  ( 0.000000000000000000, 0.000000000000000000, 11.00000000000000000 ) ) ;
#24610=( NAMED_UNIT ( * ) PLANE_ANGLE_UNIT ( ) SI_UNIT ( $, .RADIAN. ) );
#24907=VERTEX_POINT ( 'NONE', #48285 ) ;
#24918=AXIS2_PLACEMENT_3D ( 'NONE', #2815, #72596, #21274 ) ;
#25093=DIRECTION ( 'NONE',  ( -0.000000000000000000, 1.000000000000000000, -0.000000000000000000 ) ) ;
#25289=EDGE_LOOP ( 'NONE', ( #68511, #9796 ) ) ;
#25826=VERTEX_POINT ( 'NONE', #57528 ) ;
#26283=VERTEX_POINT ( 'NONE', #24098 ) ;
#26784=PLANE ( 'NONE',  #41368 ) ;
#28333=CARTESIAN_POINT ( 'NONE',  ( 0.000000000000000000, -3.149999999999999911, 0.000000000000000000 ) ) ;
#28816=ADVANCED_FACE ( 'NONE', ( #7401 ), #53056, .T. ) ;
#29056=EDGE_CURVE ( 'NONE', #24907, #25826, #39044, .T. ) ;
#29089=CARTESIAN_POINT ( 'NONE',  ( 2.265596578422603396E-15, 0.000000000000000000, -18.50000000000000000 ) ) ;
#31942=DIRECTION ( 'NONE',  ( -0.000000000000000000, 1.000000000000000000, -0.000000000000000000 ) ) ;
#32132=EDGE_CURVE ( 'NONE', #26283, #25826, #16956, .T. ) ;
#32247=DIRECTION ( 'NONE',  ( -0.000000000000000000, 1.000000000000000000, -0.000000000000000000 ) ) ;
#32453=PRODUCT ( 'plain washer (type a)_is_IS 2016 A- 22', 'plain washer (type a)_is_IS 2016 A- 22', '', ( #61810 ) ) ;
#33044=ORIENTED_EDGE ( 'NONE', *, *, #46505, .F. ) ;
#33258=DIRECTION ( 'NONE',  ( -0.000000000000000000, 1.000000000000000000, -0.000000000000000000 ) ) ;
#33641=DIRECTION ( 'NONE',  ( 0.000000000000000000, 0.000000000000000000, 1.000000000000000000 ) ) ;
#33711=AXIS2_PLACEMENT_3D ( 'NONE', #64907, #65274, #58528 ) ;
#33807=VERTEX_POINT ( 'NONE', #55017 ) ;
#34030=LINE ( 'NONE', #29089, #43982 ) ;
#34459=DIRECTION ( 'NONE',  ( 1.000000000000000000, 0.000000000000000000, 0.000000000000000000 ) ) ;
#34971=VECTOR ( 'NONE', #56035, 1000.000000000000000 ) ;
#35585=( NAMED_UNIT ( * ) SI_UNIT ( $, .STERADIAN. ) SOLID_ANGLE_UNIT ( ) );
#35937=VERTEX_POINT ( 'NONE', #13759 ) ;
#36442=DIRECTION ( 'NONE',  ( -0.000000000000000000, 1.000000000000000000, -0.000000000000000000 ) ) ;
#36809=DIRECTION ( 'NONE',  ( 0.000000000000000000, 0.000000000000000000, 1.000000000000000000 ) ) ;
#36855=ORIENTED_EDGE ( 'NONE', *, *, #32132, .T. ) ;
#38983=ADVANCED_BREP_SHAPE_REPRESENTATION ( '', ( #40499, #57354 ), #1968 ) ;
#39044=LINE ( 'NONE', #56397, #34971 ) ;
#39273=CARTESIAN_POINT ( 'NONE',  ( 0.000000000000000000, 0.000000000000000000, 11.00000000000000000 ) ) ;
#39285=DIRECTION ( 'NONE',  ( -0.000000000000000000, 1.000000000000000000, -0.000000000000000000 ) ) ;
#39985=APPLICATION_CONTEXT ( 'automotive_design' ) ;
#40214=EDGE_CURVE ( 'NONE', #61038, #35937, #41837, .T. ) ;
#40289=SHAPE_DEFINITION_REPRESENTATION ( #72807, #61424 ) ;
#40438=CIRCLE ( 'NONE', #47625, 11.00000000000000000 ) ;
#40499=MANIFOLD_SOLID_BREP ( 'BaseBody', #53899 ) ;
#40926=EDGE_LOOP ( 'NONE', ( #56854, #59703, #52169, #58202 ) ) ;
#41368=AXIS2_PLACEMENT_3D ( 'NONE', #72817, #21124, #44146 ) ;
#41776=FACE_OUTER_BOUND ( 'NONE', #40926, .T. ) ;
#41837=CIRCLE ( 'NONE', #24918, 18.50000000000000000 ) ;
#42185=ORIENTED_EDGE ( 'NONE', *, *, #42577, .F. ) ;
#42471=DIRECTION ( 'NONE',  ( -0.000000000000000000, 1.000000000000000000, -0.000000000000000000 ) ) ;
#42577=EDGE_CURVE ( 'NONE', #69767, #33807, #61284, .T. ) ;
#43248=DIRECTION ( 'NONE',  ( -0.000000000000000000, 1.000000000000000000, -0.000000000000000000 ) ) ;
#43805=ORIENTED_EDGE ( 'NONE', *, *, #73386, .F. ) ;
#43815=EDGE_CURVE ( 'NONE', #69767, #61038, #73346, .T. ) ;
#43982=VECTOR ( 'NONE', #12100, 1000.000000000000000 ) ;
#44146=DIRECTION ( 'NONE',  ( 0.000000000000000000, -0.000000000000000000, -1.000000000000000000 ) ) ;
#44941=ADVANCED_FACE ( 'NONE', ( #47736 ), #1746, .F. ) ;
#45471=DIRECTION ( 'NONE',  ( 0.000000000000000000, 0.000000000000000000, 1.000000000000000000 ) ) ;
#45951=CYLINDRICAL_SURFACE ( 'NONE', #63203, 18.50000000000000000 ) ;
#46029=SHAPE_REPRESENTATION_RELATIONSHIP ( 'NONE' , 'NONE' ,  #61424, #38983 ) ;
#46505=EDGE_CURVE ( 'NONE', #33807, #69767, #14600, .T. ) ;
#46696=ORIENTED_EDGE ( 'NONE', *, *, #73386, .T. ) ;
#47453=CARTESIAN_POINT ( 'NONE',  ( 0.000000000000000000, -3.149999999999999911, 11.00000000000000000 ) ) ;
#47625=AXIS2_PLACEMENT_3D ( 'NONE', #10471, #73839, #22145 ) ;
#47736=FACE_OUTER_BOUND ( 'NONE', #50270, .T. ) ;
#48221=VECTOR ( 'NONE', #33258, 1000.000000000000000 ) ;
#48285=CARTESIAN_POINT ( 'NONE',  ( 1.347111479062088405E-15, -3.149999999999999911, -11.00000000000000000 ) ) ;
#48334=ORIENTED_EDGE ( 'NONE', *, *, #40214, .T. ) ;
#49294=AXIS2_PLACEMENT_3D ( 'NONE', #52265, #51137, #45471 ) ;
#50097=ORIENTED_EDGE ( 'NONE', *, *, #29056, .F. ) ;
#50270=EDGE_LOOP ( 'NONE', ( #50097, #43805, #2536, #36855 ) ) ;
#50398=AXIS2_PLACEMENT_3D ( 'NONE', #28333, #39285, #33641 ) ;
#51137=DIRECTION ( 'NONE',  ( -0.000000000000000000, 1.000000000000000000, -0.000000000000000000 ) ) ;
#51994=CARTESIAN_POINT ( 'NONE',  ( 0.000000000000000000, 0.000000000000000000, 0.000000000000000000 ) ) ;
#52169=ORIENTED_EDGE ( 'NONE', *, *, #40214, .F. ) ;
#52265=CARTESIAN_POINT ( 'NONE',  ( 0.000000000000000000, -3.149999999999999911, 0.000000000000000000 ) ) ;
#52717=AXIS2_PLACEMENT_3D ( 'NONE', #67391, #43248, #55714 ) ;
#53056=CYLINDRICAL_SURFACE ( 'NONE', #8379, 18.50000000000000000 ) ;
#53272=EDGE_CURVE ( 'NONE', #24907, #20010, #64923, .T. ) ;
#53732=ADVANCED_FACE ( 'NONE', ( #18030, #62933 ), #1071, .T. ) ;
#53899=CLOSED_SHELL ( 'NONE', ( #66345, #55306, #44941, #53732, #28816, #62794 ) ) ;
#54185=DIRECTION ( 'NONE',  ( 0.000000000000000000, 0.000000000000000000, 1.000000000000000000 ) ) ;
#54728=FACE_OUTER_BOUND ( 'NONE', #4264, .T. ) ;
#54872=DIRECTION ( 'NONE',  ( -0.000000000000000000, 1.000000000000000000, -0.000000000000000000 ) ) ;
#54914=ORIENTED_EDGE ( 'NONE', *, *, #43815, .T. ) ;
#55017=CARTESIAN_POINT ( 'NONE',  ( 2.265596578422603396E-15, -3.149999999999999911, -18.50000000000000000 ) ) ;
#55306=ADVANCED_FACE ( 'NONE', ( #18155 ), #23815, .F. ) ;
#55470=FACE_BOUND ( 'NONE', #56716, .T. ) ;
#55714=DIRECTION ( 'NONE',  ( 0.000000000000000000, 0.000000000000000000, 1.000000000000000000 ) ) ;
#56035=DIRECTION ( 'NONE',  ( -0.000000000000000000, 1.000000000000000000, -0.000000000000000000 ) ) ;
#56336=STYLED_ITEM('',(#74706),#40499);
#56397=CARTESIAN_POINT ( 'NONE',  ( 1.347111479062088405E-15, 0.000000000000000000, -11.00000000000000000 ) ) ;
#56716=EDGE_LOOP ( 'NONE', ( #46696, #66577 ) ) ;
#56854=ORIENTED_EDGE ( 'NONE', *, *, #42577, .T. ) ;
#56918=DIRECTION ( 'NONE',  ( 0.000000000000000000, 0.000000000000000000, 1.000000000000000000 ) ) ;
#57354=AXIS2_PLACEMENT_3D ( 'NONE', #63097, #11422, #34459 ) ;
#57528=CARTESIAN_POINT ( 'NONE',  ( 1.347111479062088405E-15, 0.000000000000000000, -11.00000000000000000 ) ) ;
#58202=ORIENTED_EDGE ( 'NONE', *, *, #43815, .F. ) ;
#58528=DIRECTION ( 'NONE',  ( 0.000000000000000000, 0.000000000000000000, 1.000000000000000000 ) ) ;
#58834=EDGE_CURVE ( 'NONE', #20010, #26283, #21905, .T. ) ;
#59703=ORIENTED_EDGE ( 'NONE', *, *, #71135, .T. ) ;
#60402=ORIENTED_EDGE ( 'NONE', *, *, #29056, .T. ) ;
#60574=EDGE_LOOP ( 'NONE', ( #18099, #70202, #54914, #65076 ) ) ;
#61038=VERTEX_POINT ( 'NONE', #7933 ) ;
#61044=PRODUCT_DEFINITION_FORMATION_WITH_SPECIFIED_SOURCE ( 'ANY', '', #32453, .NOT_KNOWN. ) ;
#61284=CIRCLE ( 'NONE', #50398, 18.50000000000000000 ) ;
#61367=ORIENTED_EDGE ( 'NONE', *, *, #36, .T. ) ;
#61424=SHAPE_REPRESENTATION ( 'plain washer (type a)_is_IS 2016 A- 22', ( #57354 ), #1968 ) ;
#61810=PRODUCT_CONTEXT ( 'NONE', #39985, 'mechanical' ) ;
#62794=ADVANCED_FACE ( 'NONE', ( #55470, #54728 ), #26784, .T. ) ;
#62933=FACE_BOUND ( 'NONE', #25289, .T. ) ;
#63097=CARTESIAN_POINT ( 'NONE',  ( 0.000000000000000000, 0.000000000000000000, 0.000000000000000000 ) ) ;
#63203=AXIS2_PLACEMENT_3D ( 'NONE', #51994, #31942, #14572 ) ;
#63216=CARTESIAN_POINT ( 'NONE',  ( 0.000000000000000000, 0.000000000000000000, 0.000000000000000000 ) ) ;
#64509=UNCERTAINTY_MEASURE_WITH_UNIT (LENGTH_MEASURE( 1.000000000000000082E-05 ), #4941, 'distance_accuracy_value', 'NONE');
#64907=CARTESIAN_POINT ( 'NONE',  ( 0.000000000000000000, 0.000000000000000000, 0.000000000000000000 ) ) ;
#64923=CIRCLE ( 'NONE', #49294, 11.00000000000000000 ) ;
#65076=ORIENTED_EDGE ( 'NONE', *, *, #36, .F. ) ;
#65274=DIRECTION ( 'NONE',  ( -0.000000000000000000, 1.000000000000000000, -0.000000000000000000 ) ) ;
#66345=ADVANCED_FACE ( 'NONE', ( #41776 ), #45951, .T. ) ;
#66577=ORIENTED_EDGE ( 'NONE', *, *, #53272, .T. ) ;
#67391=CARTESIAN_POINT ( 'NONE',  ( 0.000000000000000000, 0.000000000000000000, 0.000000000000000000 ) ) ;
#67832=ORIENTED_EDGE ( 'NONE', *, *, #58834, .F. ) ;
#68299=( NAMED_UNIT ( * ) SI_UNIT ( $, .STERADIAN. ) SOLID_ANGLE_UNIT ( ) );
#68387=( GEOMETRIC_REPRESENTATION_CONTEXT ( 3 ) GLOBAL_UNCERTAINTY_ASSIGNED_CONTEXT ( ( #12135 ) ) GLOBAL_UNIT_ASSIGNED_CONTEXT ( ( #5423, #24610, #35585 ) ) REPRESENTATION_CONTEXT ( 'NONE', 'WORKASPACE' ) );
#68511=ORIENTED_EDGE ( 'NONE', *, *, #32132, .F. ) ;
#68940=PRODUCT_DEFINITION_CONTEXT ( 'detailed design', #71235, 'design' ) ;
#69767=VERTEX_POINT ( 'NONE', #9398 ) ;
#70026=AXIS2_PLACEMENT_3D ( 'NONE', #63216, #74167, #5893 ) ;
#70202=ORIENTED_EDGE ( 'NONE', *, *, #46505, .T. ) ;
#70760=CARTESIAN_POINT ( 'NONE',  ( 0.000000000000000000, 0.000000000000000000, 0.000000000000000000 ) ) ;
#71135=EDGE_CURVE ( 'NONE', #33807, #35937, #34030, .T. ) ;
#71235=APPLICATION_CONTEXT ( 'automotive_design' ) ;
#71982=MECHANICAL_DESIGN_GEOMETRIC_PRESENTATION_REPRESENTATION('',(#56336),#68387);
#72214=CARTESIAN_POINT ( 'NONE',  ( 0.000000000000000000, 0.000000000000000000, 18.50000000000000000 ) ) ;
#72586=DIRECTION ( 'NONE',  ( 0.000000000000000000, 0.000000000000000000, 1.000000000000000000 ) ) ;
#72596=DIRECTION ( 'NONE',  ( -0.000000000000000000, 1.000000000000000000, -0.000000000000000000 ) ) ;
#72807=PRODUCT_DEFINITION_SHAPE ( 'NONE', 'NONE',  #15017 ) ;
#72817=CARTESIAN_POINT ( 'NONE',  ( 11.00000000000000000, -3.149999999999999911, 0.000000000000000000 ) ) ;
#73180=CIRCLE ( 'NONE', #52717, 18.50000000000000000 ) ;
#73346=LINE ( 'NONE', #72214, #4696 ) ;
#73386=EDGE_CURVE ( 'NONE', #20010, #24907, #40438, .T. ) ;
#73624=CIRCLE ( 'NONE', #70026, 11.00000000000000000 ) ;
#73756=AXIS2_PLACEMENT_3D ( 'NONE', #70760, #25093, #19076 ) ;
#73839=DIRECTION ( 'NONE',  ( -0.000000000000000000, 1.000000000000000000, -0.000000000000000000 ) ) ;
#74167=DIRECTION ( 'NONE',  ( -0.000000000000000000, 1.000000000000000000, -0.000000000000000000 ) ) ;
#74700=COLOUR_RGB('Black',0.12,0.14,0.17);
#74701=FILL_AREA_STYLE_COLOUR('',#74700);
#74702=FILL_AREA_STYLE('',(#74701));
#74703=SURFACE_STYLE_FILL_AREA(#74702);
#74704=SURFACE_SIDE_STYLE('',(#74703));
#74705=SURFACE_STYLE_USAGE(.BOTH.,#74704);
#74706=PRESENTATION_STYLE_ASSIGNMENT((#74705));
ENDSEC;
END-ISO-10303-21;
